ISO-10303-21;
HEADER;
/* Generated by software containing ST-Developer
 * from STEP Tools, Inc. (www.steptools.com) 
 */

FILE_DESCRIPTION(
/* description */ ('Hand-crank flanged shaft unit'),
/* implementation_level */ '2;1');

FILE_NAME(
/* name */ 'Flange bolt sleeve.step',
/* time_stamp */ '2026-10-27T18:35:45-07:00',
/* author */ (''),
/* organization */ (''),
/* preprocessor_version */ 'ST-DEVELOPER v20.2',
/* originating_system */ 'Autodesk Translation Framework v15.17.0.0',
/* authorisation */ '');

FILE_SCHEMA (('AUTOMOTIVE_DESIGN { 1 0 10303 214 3 1 1 }'));
ENDSEC;

DATA;
#10=MECHANICAL_DESIGN_GEOMETRIC_PRESENTATION_REPRESENTATION('',(#280),#6805);
#240=SHAPE_REPRESENTATION_RELATIONSHIP('SRR','None',#6901,#260);
#260=ADVANCED_BREP_SHAPE_REPRESENTATION('',(#301),#6784);
#280=STYLED_ITEM('',(#7098),#301);
#301=MANIFOLD_SOLID_BREP('Body1',#3321);
#342=FACE_BOUND('',#754,.T.);
#343=FACE_BOUND('',#756,.T.);
#426=PLANE('',#3608);
#427=PLANE('',#3609);
#541=FACE_OUTER_BOUND('',#751,.T.);
#542=FACE_OUTER_BOUND('',#752,.T.);
#543=FACE_OUTER_BOUND('',#753,.T.);
#544=FACE_OUTER_BOUND('',#755,.T.);
#751=EDGE_LOOP('',(#2383,#2384,#2385,#2386));
#752=EDGE_LOOP('',(#2387,#2388,#2389,#2390));
#753=EDGE_LOOP('',(#2391));
#754=EDGE_LOOP('',(#2392));
#755=EDGE_LOOP('',(#2393));
#756=EDGE_LOOP('',(#2394));
#1027=LINE('',#5076,#1255);
#1028=LINE('',#5082,#1256);
#1255=VECTOR('',#4086,0.425);
#1256=VECTOR('',#4093,0.595);
#1457=CIRCLE('',#3603,0.425);
#1458=CIRCLE('',#3604,0.425);
#1459=CIRCLE('',#3606,0.595);
#1460=CIRCLE('',#3607,0.595);
#1613=VERTEX_POINT('',#5073);
#1614=VERTEX_POINT('',#5075);
#1615=VERTEX_POINT('',#5079);
#1616=VERTEX_POINT('',#5081);
#1909=EDGE_CURVE('',#1613,#1613,#1457,.T.);
#1910=EDGE_CURVE('',#1613,#1614,#1027,.T.);
#1911=EDGE_CURVE('',#1614,#1614,#1458,.T.);
#1912=EDGE_CURVE('',#1615,#1615,#1459,.T.);
#1913=EDGE_CURVE('',#1615,#1616,#1028,.T.);
#1914=EDGE_CURVE('',#1616,#1616,#1460,.T.);
#2383=ORIENTED_EDGE('',*,*,#1909,.F.);
#2384=ORIENTED_EDGE('',*,*,#1910,.T.);
#2385=ORIENTED_EDGE('',*,*,#1911,.T.);
#2386=ORIENTED_EDGE('',*,*,#1910,.F.);
#2387=ORIENTED_EDGE('',*,*,#1912,.F.);
#2388=ORIENTED_EDGE('',*,*,#1913,.T.);
#2389=ORIENTED_EDGE('',*,*,#1914,.T.);
#2390=ORIENTED_EDGE('',*,*,#1913,.F.);
#2391=ORIENTED_EDGE('',*,*,#1912,.T.);
#2392=ORIENTED_EDGE('',*,*,#1909,.T.);
#2393=ORIENTED_EDGE('',*,*,#1914,.F.);
#2394=ORIENTED_EDGE('',*,*,#1911,.F.);
#3077=CYLINDRICAL_SURFACE('',#3602,0.425);
#3078=CYLINDRICAL_SURFACE('',#3605,0.595);
#3158=ADVANCED_FACE('',(#541),#3077,.F.);
#3159=ADVANCED_FACE('',(#542),#3078,.T.);
#3160=ADVANCED_FACE('',(#543,#342),#426,.T.);
#3161=ADVANCED_FACE('',(#544,#343),#427,.F.);
#3321=CLOSED_SHELL('',(#3158,#3159,#3160,#3161));
#3601=AXIS2_PLACEMENT_3D('',#5071,#4080,#4081);
#3602=AXIS2_PLACEMENT_3D('',#5072,#4082,#4083);
#3603=AXIS2_PLACEMENT_3D('',#5074,#4084,#4085);
#3604=AXIS2_PLACEMENT_3D('',#5077,#4087,#4088);
#3605=AXIS2_PLACEMENT_3D('',#5078,#4089,#4090);
#3606=AXIS2_PLACEMENT_3D('',#5080,#4091,#4092);
#3607=AXIS2_PLACEMENT_3D('',#5083,#4094,#4095);
#3608=AXIS2_PLACEMENT_3D('',#5084,#4096,#4097);
#3609=AXIS2_PLACEMENT_3D('',#5085,#4098,#4099);
#4080=DIRECTION('axis',(0.,0.,1.));
#4081=DIRECTION('refdir',(1.,0.,0.));
#4082=DIRECTION('center_axis',(0.,1.,0.));
#4083=DIRECTION('ref_axis',(1.,0.,0.));
#4084=DIRECTION('center_axis',(0.,-1.,0.));
#4085=DIRECTION('ref_axis',(1.,0.,0.));
#4086=DIRECTION('',(0.,-1.,0.));
#4087=DIRECTION('center_axis',(0.,-1.,0.));
#4088=DIRECTION('ref_axis',(1.,0.,0.));
#4089=DIRECTION('center_axis',(0.,1.,0.));
#4090=DIRECTION('ref_axis',(1.,0.,0.));
#4091=DIRECTION('center_axis',(0.,1.,0.));
#4092=DIRECTION('ref_axis',(1.,0.,0.));
#4093=DIRECTION('',(0.,-1.,0.));
#4094=DIRECTION('center_axis',(0.,1.,0.));
#4095=DIRECTION('ref_axis',(1.,0.,0.));
#4096=DIRECTION('center_axis',(0.,1.,0.));
#4097=DIRECTION('ref_axis',(1.,0.,0.));
#4098=DIRECTION('center_axis',(0.,1.,0.));
#4099=DIRECTION('ref_axis',(1.,0.,0.));
#5071=CARTESIAN_POINT('',(0.,0.,0.));
#5072=CARTESIAN_POINT('Origin',(-3.2,-1.,4.3));
#5073=CARTESIAN_POINT('',(-3.625,0.,4.3));
#5074=CARTESIAN_POINT('Origin',(-3.2,0.,4.3));
#5075=CARTESIAN_POINT('',(-3.625,-1.,4.3));
#5076=CARTESIAN_POINT('',(-3.625,-1.,4.3));
#5077=CARTESIAN_POINT('Origin',(-3.2,-1.,4.3));
#5078=CARTESIAN_POINT('Origin',(-3.2,-1.,4.3));
#5079=CARTESIAN_POINT('',(-3.795,0.,4.3));
#5080=CARTESIAN_POINT('Origin',(-3.2,0.,4.3));
#5081=CARTESIAN_POINT('',(-3.795,-1.,4.3));
#5082=CARTESIAN_POINT('',(-3.795,-1.,4.3));
#5083=CARTESIAN_POINT('Origin',(-3.2,-1.,4.3));
#5084=CARTESIAN_POINT('Origin',(-3.2,0.,4.3));
#5085=CARTESIAN_POINT('Origin',(-3.2,-1.,4.3));
#6759=UNCERTAINTY_MEASURE_WITH_UNIT(LENGTH_MEASURE(0.001),#6806,
'DISTANCE_ACCURACY_VALUE',
'Maximum model space distance between geometric entities at asserted c
onnectivities');
#6780=UNCERTAINTY_MEASURE_WITH_UNIT(LENGTH_MEASURE(0.001),#6806,
'DISTANCE_ACCURACY_VALUE',
'Maximum model space distance between geometric entities at asserted c
onnectivities');
#6784=(
GEOMETRIC_REPRESENTATION_CONTEXT(3)
GLOBAL_UNCERTAINTY_ASSIGNED_CONTEXT((#6759))
GLOBAL_UNIT_ASSIGNED_CONTEXT((#6806,#6808,#6809))
REPRESENTATION_CONTEXT('','3D')
);
#6805=(
GEOMETRIC_REPRESENTATION_CONTEXT(3)
GLOBAL_UNCERTAINTY_ASSIGNED_CONTEXT((#6780))
GLOBAL_UNIT_ASSIGNED_CONTEXT((#6806,#6808,#6809))
REPRESENTATION_CONTEXT('','3D')
);
#6806=(
LENGTH_UNIT()
NAMED_UNIT(*)
SI_UNIT(.CENTI.,.METRE.)
);
#6808=(
NAMED_UNIT(*)
PLANE_ANGLE_UNIT()
SI_UNIT($,.RADIAN.)
);
#6809=(
NAMED_UNIT(*)
SI_UNIT($,.STERADIAN.)
SOLID_ANGLE_UNIT()
);
#6813=SHAPE_DEFINITION_REPRESENTATION(#6837,#6901);
#6837=PRODUCT_DEFINITION_SHAPE('',$,#6926);
#6901=SHAPE_REPRESENTATION('',(#3601),#6784);
#6922=PRODUCT_DEFINITION_CONTEXT('part definition',#6996,'design');
#6926=PRODUCT_DEFINITION('Flange bolt sleeve','Flange bolt sleeve',#6950,
#6922);
#6950=PRODUCT_DEFINITION_FORMATION('',$,#7001);
#6996=APPLICATION_CONTEXT(
'Core Data for Automotive Mechanical Design Process');
#6997=PRODUCT_CONTEXT('part definition',#6996,'mechanical');
#7001=PRODUCT('Flange bolt sleeve','Flange bolt sleeve',
'Flange bolt sleeve',(#6997));
#7092=COLOUR_RGB('Black',0.12,0.14,0.17);
#7093=FILL_AREA_STYLE_COLOUR('',#7092);
#7094=FILL_AREA_STYLE('',(#7093));
#7095=SURFACE_STYLE_FILL_AREA(#7094);
#7096=SURFACE_SIDE_STYLE('',(#7095));
#7097=SURFACE_STYLE_USAGE(.BOTH.,#7096);
#7098=PRESENTATION_STYLE_ASSIGNMENT((#7097));
ENDSEC;
END-ISO-10303-21;
